ISO-10303-21;
HEADER;
/* Generated by software containing ST-Developer
 * from STEP Tools, Inc. (www.steptools.com) 
 */

FILE_DESCRIPTION(
/* description */ ('STEP AP214'),
/* implementation_level */ '2;1');

FILE_NAME(
/* name */ 'Coupling Set Screw.step',
/* time_stamp */ '2026-11-15T14:49:54-08:00',
/* author */ (''),
/* organization */ (''),
/* preprocessor_version */ 'ST-DEVELOPER v20.2',
/* originating_system */ 'Autodesk Translation Framework v15.17.0.0',
/* authorisation */ '');

FILE_SCHEMA (('AUTOMOTIVE_DESIGN { 1 0 10303 214 3 1 1 }'));
ENDSEC;

DATA;
#10=MECHANICAL_DESIGN_GEOMETRIC_PRESENTATION_REPRESENTATION('',(#1116),#66721);
#1054=SHAPE_REPRESENTATION_RELATIONSHIP('SRR','None',#66917,#1085);
#1085=ADVANCED_BREP_SHAPE_REPRESENTATION('',(#1151),#66708);
#1116=STYLED_ITEM('',(#67095),#1151);
#1151=MANIFOLD_SOLID_BREP('Body1',#25682);
#1403=FACE_BOUND('',#4993,.T.);
#2026=PLANE('',#27945);
#2027=PLANE('',#27947);
#2028=PLANE('',#27950);
#2029=PLANE('',#27951);
#2030=PLANE('',#27952);
#2031=PLANE('',#27953);
#2032=PLANE('',#27954);
#2033=PLANE('',#27955);
#2034=PLANE('',#27956);
#3315=FACE_OUTER_BOUND('',#4992,.T.);
#3316=FACE_OUTER_BOUND('',#4994,.T.);
#3317=FACE_OUTER_BOUND('',#4995,.T.);
#3318=FACE_OUTER_BOUND('',#4996,.T.);
#3319=FACE_OUTER_BOUND('',#4997,.T.);
#3320=FACE_OUTER_BOUND('',#4998,.T.);
#3321=FACE_OUTER_BOUND('',#4999,.T.);
#3322=FACE_OUTER_BOUND('',#5000,.T.);
#3323=FACE_OUTER_BOUND('',#5001,.T.);
#3324=FACE_OUTER_BOUND('',#5002,.T.);
#4992=EDGE_LOOP('',(#21926));
#4993=EDGE_LOOP('',(#21927,#21928,#21929,#21930,#21931,#21932));
#4994=EDGE_LOOP('',(#21933));
#4995=EDGE_LOOP('',(#21934,#21935,#21936,#21937));
#4996=EDGE_LOOP('',(#21938,#21939,#21940,#21941,#21942,#21943));
#4997=EDGE_LOOP('',(#21944,#21945,#21946,#21947));
#4998=EDGE_LOOP('',(#21948,#21949,#21950,#21951));
#4999=EDGE_LOOP('',(#21952,#21953,#21954,#21955));
#5000=EDGE_LOOP('',(#21956,#21957,#21958,#21959));
#5001=EDGE_LOOP('',(#21960,#21961,#21962,#21963));
#5002=EDGE_LOOP('',(#21964,#21965,#21966,#21967));
#6901=LINE('',#64021,#8890);
#6902=LINE('',#64023,#8891);
#6903=LINE('',#64025,#8892);
#6904=LINE('',#64027,#8893);
#6905=LINE('',#64029,#8894);
#6906=LINE('',#64030,#8895);
#6907=LINE('',#64035,#8896);
#6908=LINE('',#64039,#8897);
#6909=LINE('',#64041,#8898);
#6910=LINE('',#64043,#8899);
#6911=LINE('',#64045,#8900);
#6912=LINE('',#64047,#8901);
#6913=LINE('',#64048,#8902);
#6914=LINE('',#64050,#8903);
#6915=LINE('',#64051,#8904);
#6916=LINE('',#64053,#8905);
#6917=LINE('',#64055,#8906);
#6918=LINE('',#64057,#8907);
#6919=LINE('',#64059,#8908);
#8890=VECTOR('',#33986,1000.);
#8891=VECTOR('',#33987,1000.);
#8892=VECTOR('',#33988,1000.);
#8893=VECTOR('',#33989,1000.);
#8894=VECTOR('',#33990,1000.);
#8895=VECTOR('',#33991,1000.);
#8896=VECTOR('',#33998,2.5);
#8897=VECTOR('',#34001,1000.);
#8898=VECTOR('',#34002,1000.);
#8899=VECTOR('',#34003,1000.);
#8900=VECTOR('',#34004,1000.);
#8901=VECTOR('',#34005,1000.);
#8902=VECTOR('',#34006,1000.);
#8903=VECTOR('',#34009,1000.);
#8904=VECTOR('',#34010,1000.);
#8905=VECTOR('',#34013,1000.);
#8906=VECTOR('',#34016,1000.);
#8907=VECTOR('',#34019,1000.);
#8908=VECTOR('',#34022,1000.);
#10341=CIRCLE('',#27946,2.5);
#10342=CIRCLE('',#27948,2.5);
#12361=VERTEX_POINT('',#64017);
#12362=VERTEX_POINT('',#64019);
#12363=VERTEX_POINT('',#64020);
#12364=VERTEX_POINT('',#64022);
#12365=VERTEX_POINT('',#64024);
#12366=VERTEX_POINT('',#64026);
#12367=VERTEX_POINT('',#64028);
#12368=VERTEX_POINT('',#64032);
#12369=VERTEX_POINT('',#64037);
#12370=VERTEX_POINT('',#64038);
#12371=VERTEX_POINT('',#64040);
#12372=VERTEX_POINT('',#64042);
#12373=VERTEX_POINT('',#64044);
#12374=VERTEX_POINT('',#64046);
#15656=EDGE_CURVE('',#12361,#12361,#10341,.T.);
#15657=EDGE_CURVE('',#12362,#12363,#6901,.T.);
#15658=EDGE_CURVE('',#12363,#12364,#6902,.T.);
#15659=EDGE_CURVE('',#12364,#12365,#6903,.T.);
#15660=EDGE_CURVE('',#12365,#12366,#6904,.T.);
#15661=EDGE_CURVE('',#12366,#12367,#6905,.T.);
#15662=EDGE_CURVE('',#12367,#12362,#6906,.T.);
#15663=EDGE_CURVE('',#12368,#12368,#10342,.T.);
#15664=EDGE_CURVE('',#12361,#12368,#6907,.T.);
#15665=EDGE_CURVE('',#12369,#12370,#6908,.T.);
#15666=EDGE_CURVE('',#12371,#12369,#6909,.T.);
#15667=EDGE_CURVE('',#12372,#12371,#6910,.T.);
#15668=EDGE_CURVE('',#12373,#12372,#6911,.T.);
#15669=EDGE_CURVE('',#12374,#12373,#6912,.T.);
#15670=EDGE_CURVE('',#12370,#12374,#6913,.T.);
#15671=EDGE_CURVE('',#12369,#12367,#6914,.T.);
#15672=EDGE_CURVE('',#12370,#12362,#6915,.T.);
#15673=EDGE_CURVE('',#12371,#12366,#6916,.T.);
#15674=EDGE_CURVE('',#12372,#12365,#6917,.T.);
#15675=EDGE_CURVE('',#12373,#12364,#6918,.T.);
#15676=EDGE_CURVE('',#12374,#12363,#6919,.T.);
#21926=ORIENTED_EDGE('',*,*,#15656,.T.);
#21927=ORIENTED_EDGE('',*,*,#15657,.T.);
#21928=ORIENTED_EDGE('',*,*,#15658,.T.);
#21929=ORIENTED_EDGE('',*,*,#15659,.T.);
#21930=ORIENTED_EDGE('',*,*,#15660,.T.);
#21931=ORIENTED_EDGE('',*,*,#15661,.T.);
#21932=ORIENTED_EDGE('',*,*,#15662,.T.);
#21933=ORIENTED_EDGE('',*,*,#15663,.T.);
#21934=ORIENTED_EDGE('',*,*,#15656,.F.);
#21935=ORIENTED_EDGE('',*,*,#15664,.T.);
#21936=ORIENTED_EDGE('',*,*,#15663,.F.);
#21937=ORIENTED_EDGE('',*,*,#15664,.F.);
#21938=ORIENTED_EDGE('',*,*,#15665,.F.);
#21939=ORIENTED_EDGE('',*,*,#15666,.F.);
#21940=ORIENTED_EDGE('',*,*,#15667,.F.);
#21941=ORIENTED_EDGE('',*,*,#15668,.F.);
#21942=ORIENTED_EDGE('',*,*,#15669,.F.);
#21943=ORIENTED_EDGE('',*,*,#15670,.F.);
#21944=ORIENTED_EDGE('',*,*,#15662,.F.);
#21945=ORIENTED_EDGE('',*,*,#15671,.F.);
#21946=ORIENTED_EDGE('',*,*,#15665,.T.);
#21947=ORIENTED_EDGE('',*,*,#15672,.T.);
#21948=ORIENTED_EDGE('',*,*,#15661,.F.);
#21949=ORIENTED_EDGE('',*,*,#15673,.F.);
#21950=ORIENTED_EDGE('',*,*,#15666,.T.);
#21951=ORIENTED_EDGE('',*,*,#15671,.T.);
#21952=ORIENTED_EDGE('',*,*,#15660,.F.);
#21953=ORIENTED_EDGE('',*,*,#15674,.F.);
#21954=ORIENTED_EDGE('',*,*,#15667,.T.);
#21955=ORIENTED_EDGE('',*,*,#15673,.T.);
#21956=ORIENTED_EDGE('',*,*,#15659,.F.);
#21957=ORIENTED_EDGE('',*,*,#15675,.F.);
#21958=ORIENTED_EDGE('',*,*,#15668,.T.);
#21959=ORIENTED_EDGE('',*,*,#15674,.T.);
#21960=ORIENTED_EDGE('',*,*,#15658,.F.);
#21961=ORIENTED_EDGE('',*,*,#15676,.F.);
#21962=ORIENTED_EDGE('',*,*,#15669,.T.);
#21963=ORIENTED_EDGE('',*,*,#15675,.T.);
#21964=ORIENTED_EDGE('',*,*,#15657,.F.);
#21965=ORIENTED_EDGE('',*,*,#15672,.F.);
#21966=ORIENTED_EDGE('',*,*,#15670,.T.);
#21967=ORIENTED_EDGE('',*,*,#15676,.T.);
#24104=CYLINDRICAL_SURFACE('',#27949,2.5);
#25268=ADVANCED_FACE('',(#3315,#1403),#2026,.T.);
#25269=ADVANCED_FACE('',(#3316),#2027,.T.);
#25270=ADVANCED_FACE('',(#3317),#24104,.T.);
#25271=ADVANCED_FACE('',(#3318),#2028,.F.);
#25272=ADVANCED_FACE('',(#3319),#2029,.F.);
#25273=ADVANCED_FACE('',(#3320),#2030,.F.);
#25274=ADVANCED_FACE('',(#3321),#2031,.F.);
#25275=ADVANCED_FACE('',(#3322),#2032,.F.);
#25276=ADVANCED_FACE('',(#3323),#2033,.F.);
#25277=ADVANCED_FACE('',(#3324),#2034,.F.);
#25682=CLOSED_SHELL('',(#25268,#25269,#25270,#25271,#25272,#25273,#25274,
#25275,#25276,#25277));
#27944=AXIS2_PLACEMENT_3D('',#64015,#33980,#33981);
#27945=AXIS2_PLACEMENT_3D('',#64016,#33982,#33983);
#27946=AXIS2_PLACEMENT_3D('',#64018,#33984,#33985);
#27947=AXIS2_PLACEMENT_3D('',#64031,#33992,#33993);
#27948=AXIS2_PLACEMENT_3D('',#64033,#33994,#33995);
#27949=AXIS2_PLACEMENT_3D('',#64034,#33996,#33997);
#27950=AXIS2_PLACEMENT_3D('',#64036,#33999,#34000);
#27951=AXIS2_PLACEMENT_3D('',#64049,#34007,#34008);
#27952=AXIS2_PLACEMENT_3D('',#64052,#34011,#34012);
#27953=AXIS2_PLACEMENT_3D('',#64054,#34014,#34015);
#27954=AXIS2_PLACEMENT_3D('',#64056,#34017,#34018);
#27955=AXIS2_PLACEMENT_3D('',#64058,#34020,#34021);
#27956=AXIS2_PLACEMENT_3D('',#64060,#34023,#34024);
#33980=DIRECTION('axis',(0.,0.,1.));
#33981=DIRECTION('refdir',(1.,0.,0.));
#33982=DIRECTION('center_axis',(0.,-1.,0.));
#33983=DIRECTION('ref_axis',(0.,0.,-1.));
#33984=DIRECTION('center_axis',(0.,-1.,0.));
#33985=DIRECTION('ref_axis',(-1.,0.,0.));
#33986=DIRECTION('',(-0.866025403761798,0.,0.500000000039214));
#33987=DIRECTION('',(0.,0.,1.));
#33988=DIRECTION('',(0.866025403761798,0.,0.500000000039214));
#33989=DIRECTION('',(0.866025403761798,0.,-0.500000000039214));
#33990=DIRECTION('',(0.,0.,-1.));
#33991=DIRECTION('',(-0.866025403761798,0.,-0.500000000039214));
#33992=DIRECTION('center_axis',(0.,1.,0.));
#33993=DIRECTION('ref_axis',(1.,0.,0.));
#33994=DIRECTION('center_axis',(0.,1.,0.));
#33995=DIRECTION('ref_axis',(-1.,0.,0.));
#33996=DIRECTION('center_axis',(0.,-1.,0.));
#33997=DIRECTION('ref_axis',(-1.,0.,0.));
#33998=DIRECTION('',(0.,1.,0.));
#33999=DIRECTION('center_axis',(0.,1.,0.));
#34000=DIRECTION('ref_axis',(1.,0.,0.));
#34001=DIRECTION('',(-0.866025403761798,0.,-0.500000000039214));
#34002=DIRECTION('',(0.,0.,-1.));
#34003=DIRECTION('',(0.866025403761798,0.,-0.500000000039214));
#34004=DIRECTION('',(0.866025403761798,0.,0.500000000039214));
#34005=DIRECTION('',(0.,0.,1.));
#34006=DIRECTION('',(-0.866025403761798,0.,0.500000000039214));
#34007=DIRECTION('center_axis',(0.500000000039214,0.,-0.866025403761798));
#34008=DIRECTION('ref_axis',(0.,-1.,0.));
#34009=DIRECTION('',(0.,-1.,0.));
#34010=DIRECTION('',(0.,-1.,0.));
#34011=DIRECTION('center_axis',(1.,0.,0.));
#34012=DIRECTION('ref_axis',(0.,1.,0.));
#34013=DIRECTION('',(0.,-1.,0.));
#34014=DIRECTION('center_axis',(0.500000000039214,0.,0.866025403761798));
#34015=DIRECTION('ref_axis',(0.,-1.,0.));
#34016=DIRECTION('',(0.,-1.,0.));
#34017=DIRECTION('center_axis',(-0.500000000039214,0.,0.866025403761798));
#34018=DIRECTION('ref_axis',(0.,1.,0.));
#34019=DIRECTION('',(0.,-1.,0.));
#34020=DIRECTION('center_axis',(-1.,0.,0.));
#34021=DIRECTION('ref_axis',(0.,0.,1.));
#34022=DIRECTION('',(0.,-1.,0.));
#34023=DIRECTION('center_axis',(-0.500000000039214,0.,-0.866025403761798));
#34024=DIRECTION('ref_axis',(-0.866025403761798,0.,0.500000000039214));
#64015=CARTESIAN_POINT('',(0.,0.,0.));
#64016=CARTESIAN_POINT('Origin',(29.,-23.8,0.));
#64017=CARTESIAN_POINT('',(31.5,-23.8,-3.06161699786838E-16));
#64018=CARTESIAN_POINT('Origin',(29.,-23.8,0.));
#64019=CARTESIAN_POINT('',(29.,-23.8,-1.3856406461));
#64020=CARTESIAN_POINT('',(27.8,-23.8,-0.692820323));
#64021=CARTESIAN_POINT('',(28.3999999999746,-23.8,-1.03923048453533));
#64022=CARTESIAN_POINT('',(27.8,-23.8,0.692820323));
#64023=CARTESIAN_POINT('',(27.8,-23.8,0.17320508075));
#64024=CARTESIAN_POINT('',(29.,-23.8,1.3856406461));
#64025=CARTESIAN_POINT('',(28.3999999999746,-23.8,1.03923048453533));
#64026=CARTESIAN_POINT('',(30.2,-23.8,0.692820323));
#64027=CARTESIAN_POINT('',(29.6000000000254,-23.8,1.03923048453533));
#64028=CARTESIAN_POINT('',(30.2,-23.8,-0.692820323));
#64029=CARTESIAN_POINT('',(30.2,-23.8,0.));
#64030=CARTESIAN_POINT('',(29.6000000000254,-23.8,-1.03923048453533));
#64031=CARTESIAN_POINT('Origin',(29.,-7.8,0.));
#64032=CARTESIAN_POINT('',(31.5,-7.8,-3.06161699786838E-16));
#64033=CARTESIAN_POINT('Origin',(29.,-7.8,0.));
#64034=CARTESIAN_POINT('Origin',(29.,-15.8,0.));
#64035=CARTESIAN_POINT('',(31.5,-15.8,3.06161699786838E-16));
#64036=CARTESIAN_POINT('Origin',(29.,-21.3,3.11198878113149E-17));
#64037=CARTESIAN_POINT('',(30.2,-21.3,-0.692820323));
#64038=CARTESIAN_POINT('',(29.,-21.3,-1.3856406461));
#64039=CARTESIAN_POINT('',(30.2,-21.3,-0.692820323));
#64040=CARTESIAN_POINT('',(30.2,-21.3,0.692820323));
#64041=CARTESIAN_POINT('',(30.2,-21.3,0.692820323));
#64042=CARTESIAN_POINT('',(29.,-21.3,1.3856406461));
#64043=CARTESIAN_POINT('',(29.,-21.3,1.3856406461));
#64044=CARTESIAN_POINT('',(27.8,-21.3,0.692820323));
#64045=CARTESIAN_POINT('',(27.8,-21.3,0.692820323));
#64046=CARTESIAN_POINT('',(27.8,-21.3,-0.692820323));
#64047=CARTESIAN_POINT('',(27.8,-21.3,-0.692820323));
#64048=CARTESIAN_POINT('',(29.,-21.3,-1.3856406461));
#64049=CARTESIAN_POINT('Origin',(29.6,-21.3,-1.03923048455));
#64050=CARTESIAN_POINT('',(30.2,-21.3,-0.692820323));
#64051=CARTESIAN_POINT('',(29.,-21.3,-1.3856406461));
#64052=CARTESIAN_POINT('Origin',(30.2,-21.3,0.));
#64053=CARTESIAN_POINT('',(30.2,-21.3,0.692820323));
#64054=CARTESIAN_POINT('Origin',(29.6,-21.3,1.03923048455));
#64055=CARTESIAN_POINT('',(29.,-21.3,1.3856406461));
#64056=CARTESIAN_POINT('Origin',(28.4,-21.3,1.03923048455));
#64057=CARTESIAN_POINT('',(27.8,-21.3,0.692820323));
#64058=CARTESIAN_POINT('Origin',(27.8,-21.3,0.3464101615));
#64059=CARTESIAN_POINT('',(27.8,-21.3,-0.692820323));
#64060=CARTESIAN_POINT('Origin',(28.4,-21.3,-1.03923048455));
#66667=UNCERTAINTY_MEASURE_WITH_UNIT(LENGTH_MEASURE(0.01),#66722,
'DISTANCE_ACCURACY_VALUE',
'Maximum model space distance between geometric entities at asserted c
onnectivities');
#66680=UNCERTAINTY_MEASURE_WITH_UNIT(LENGTH_MEASURE(0.01),#66722,
'DISTANCE_ACCURACY_VALUE',
'Maximum model space distance between geometric entities at asserted c
onnectivities');
#66708=(
GEOMETRIC_REPRESENTATION_CONTEXT(3)
GLOBAL_UNCERTAINTY_ASSIGNED_CONTEXT((#66667))
GLOBAL_UNIT_ASSIGNED_CONTEXT((#66722,#66724,#66725))
REPRESENTATION_CONTEXT('','3D')
);
#66721=(
GEOMETRIC_REPRESENTATION_CONTEXT(3)
GLOBAL_UNCERTAINTY_ASSIGNED_CONTEXT((#66680))
GLOBAL_UNIT_ASSIGNED_CONTEXT((#66722,#66724,#66725))
REPRESENTATION_CONTEXT('','3D')
);
#66722=(
LENGTH_UNIT()
NAMED_UNIT(*)
SI_UNIT(.MILLI.,.METRE.)
);
#66724=(
NAMED_UNIT(*)
PLANE_ANGLE_UNIT()
SI_UNIT($,.RADIAN.)
);
#66725=(
NAMED_UNIT(*)
SI_UNIT($,.STERADIAN.)
SOLID_ANGLE_UNIT()
);
#66753=SHAPE_DEFINITION_REPRESENTATION(#66813,#66917);
#66813=PRODUCT_DEFINITION_SHAPE('',$,#66958);
#66917=SHAPE_REPRESENTATION('',(#27944),#66708);
#66930=PRODUCT_DEFINITION_CONTEXT('part definition',#67052,'design');
#66958=PRODUCT_DEFINITION('Coupling Set Screw','Coupling Set Screw',#66998,
#66930);
#66998=PRODUCT_DEFINITION_FORMATION('',$,#67081);
#67052=APPLICATION_CONTEXT(
'Core Data for Automotive Mechanical Design Process');
#67053=PRODUCT_CONTEXT('part definition',#67052,'mechanical');
#67081=PRODUCT('Coupling Set Screw','Coupling Set Screw',$,(#67053));
#67095=PRESENTATION_STYLE_ASSIGNMENT((#67097));
#67097=SURFACE_STYLE_USAGE(.BOTH.,#67099);
#67099=SURFACE_SIDE_STYLE('',(#67101));
#67101=SURFACE_STYLE_FILL_AREA(#67103);
#67103=FILL_AREA_STYLE('Opaque(202,209,238)',(#67105));
#67105=FILL_AREA_STYLE_COLOUR('Opaque(202,209,238)',#67107);
#67107=COLOUR_RGB('Opaque(202,209,238)',0.792156862745098,0.819607843137255,
0.933333333333333);
ENDSEC;
END-ISO-10303-21;
